ISO-10303-21;
HEADER;
/* Generated by software containing ST-Developer
 * from STEP Tools, Inc. (www.steptools.com) 
 */

FILE_DESCRIPTION(
/* description */ ('Hand-crank flanged shaft unit'),
/* implementation_level */ '2;1');

FILE_NAME(
/* name */ 'Socket Set Screw - M5x8.step',
/* time_stamp */ '2026-10-27T18:35:45-07:00',
/* author */ (''),
/* organization */ (''),
/* preprocessor_version */ 'ST-DEVELOPER v20.2',
/* originating_system */ 'Autodesk Translation Framework v15.17.0.0',
/* authorisation */ '');

FILE_SCHEMA (('AUTOMOTIVE_DESIGN { 1 0 10303 214 3 1 1 }'));
ENDSEC;

DATA;
#10=MECHANICAL_DESIGN_GEOMETRIC_PRESENTATION_REPRESENTATION('',(#299),#6805);
#26=CONICAL_SURFACE('',#3919,0.235,0.785398163397448);
#27=CONICAL_SURFACE('',#3923,0.2125,0.785398163397448);
#258=SHAPE_REPRESENTATION_RELATIONSHIP('SRR','None',#6921,#278);
#278=ADVANCED_BREP_SHAPE_REPRESENTATION('',(#319),#6804);
#299=STYLED_ITEM('',(#7098),#319);
#319=MANIFOLD_SOLID_BREP('Body1',#3341);
#409=FACE_BOUND('',#976,.T.);
#506=PLANE('',#3910);
#507=PLANE('',#3911);
#508=PLANE('',#3912);
#509=PLANE('',#3913);
#510=PLANE('',#3914);
#511=PLANE('',#3915);
#512=PLANE('',#3916);
#513=PLANE('',#3917);
#514=PLANE('',#3925);
#691=FACE_OUTER_BOUND('',#968,.T.);
#692=FACE_OUTER_BOUND('',#969,.T.);
#693=FACE_OUTER_BOUND('',#970,.T.);
#694=FACE_OUTER_BOUND('',#971,.T.);
#695=FACE_OUTER_BOUND('',#972,.T.);
#696=FACE_OUTER_BOUND('',#973,.T.);
#697=FACE_OUTER_BOUND('',#974,.T.);
#698=FACE_OUTER_BOUND('',#975,.T.);
#699=FACE_OUTER_BOUND('',#977,.T.);
#700=FACE_OUTER_BOUND('',#978,.T.);
#701=FACE_OUTER_BOUND('',#979,.T.);
#702=FACE_OUTER_BOUND('',#980,.T.);
#968=EDGE_LOOP('',(#3017,#3018,#3019,#3020));
#969=EDGE_LOOP('',(#3021,#3022,#3023,#3024));
#970=EDGE_LOOP('',(#3025,#3026,#3027,#3028));
#971=EDGE_LOOP('',(#3029,#3030,#3031,#3032));
#972=EDGE_LOOP('',(#3033,#3034,#3035,#3036));
#973=EDGE_LOOP('',(#3037,#3038,#3039,#3040));
#974=EDGE_LOOP('',(#3041,#3042,#3043,#3044,#3045,#3046));
#975=EDGE_LOOP('',(#3047));
#976=EDGE_LOOP('',(#3048,#3049,#3050,#3051,#3052,#3053));
#977=EDGE_LOOP('',(#3054,#3055,#3056,#3057));
#978=EDGE_LOOP('',(#3058,#3059,#3060,#3061));
#979=EDGE_LOOP('',(#3062,#3063,#3064,#3065));
#980=EDGE_LOOP('',(#3066));
#1188=LINE('',#6696,#1416);
#1189=LINE('',#6698,#1417);
#1190=LINE('',#6700,#1418);
#1191=LINE('',#6701,#1419);
#1192=LINE('',#6704,#1420);
#1193=LINE('',#6706,#1421);
#1194=LINE('',#6707,#1422);
#1195=LINE('',#6710,#1423);
#1196=LINE('',#6712,#1424);
#1197=LINE('',#6713,#1425);
#1198=LINE('',#6716,#1426);
#1199=LINE('',#6718,#1427);
#1200=LINE('',#6719,#1428);
#1201=LINE('',#6722,#1429);
#1202=LINE('',#6724,#1430);
#1203=LINE('',#6725,#1431);
#1204=LINE('',#6727,#1432);
#1205=LINE('',#6728,#1433);
#1206=LINE('',#6736,#1434);
#1207=LINE('',#6740,#1435);
#1208=LINE('',#6744,#1436);
#1416=VECTOR('',#4861,1.);
#1417=VECTOR('',#4862,1.);
#1418=VECTOR('',#4863,1.);
#1419=VECTOR('',#4864,1.);
#1420=VECTOR('',#4867,1.);
#1421=VECTOR('',#4868,1.);
#1422=VECTOR('',#4869,1.);
#1423=VECTOR('',#4872,1.);
#1424=VECTOR('',#4873,1.);
#1425=VECTOR('',#4874,1.);
#1426=VECTOR('',#4877,1.);
#1427=VECTOR('',#4878,1.);
#1428=VECTOR('',#4879,1.);
#1429=VECTOR('',#4882,1.);
#1430=VECTOR('',#4883,1.);
#1431=VECTOR('',#4884,1.);
#1432=VECTOR('',#4887,1.);
#1433=VECTOR('',#4888,1.);
#1434=VECTOR('',#4899,0.235);
#1435=VECTOR('',#4904,0.25);
#1436=VECTOR('',#4909,0.2125);
#1565=CIRCLE('',#3918,0.22);
#1566=CIRCLE('',#3920,0.24505);
#1567=CIRCLE('',#3922,0.24505);
#1568=CIRCLE('',#3924,0.175);
#1827=VERTEX_POINT('',#6694);
#1828=VERTEX_POINT('',#6695);
#1829=VERTEX_POINT('',#6697);
#1830=VERTEX_POINT('',#6699);
#1831=VERTEX_POINT('',#6703);
#1832=VERTEX_POINT('',#6705);
#1833=VERTEX_POINT('',#6709);
#1834=VERTEX_POINT('',#6711);
#1835=VERTEX_POINT('',#6715);
#1836=VERTEX_POINT('',#6717);
#1837=VERTEX_POINT('',#6721);
#1838=VERTEX_POINT('',#6723);
#1839=VERTEX_POINT('',#6731);
#1840=VERTEX_POINT('',#6734);
#1841=VERTEX_POINT('',#6738);
#1842=VERTEX_POINT('',#6742);
#2226=EDGE_CURVE('',#1827,#1828,#1188,.T.);
#2227=EDGE_CURVE('',#1827,#1829,#1189,.T.);
#2228=EDGE_CURVE('',#1829,#1830,#1190,.T.);
#2229=EDGE_CURVE('',#1828,#1830,#1191,.T.);
#2230=EDGE_CURVE('',#1831,#1827,#1192,.T.);
#2231=EDGE_CURVE('',#1831,#1832,#1193,.T.);
#2232=EDGE_CURVE('',#1832,#1829,#1194,.T.);
#2233=EDGE_CURVE('',#1833,#1831,#1195,.T.);
#2234=EDGE_CURVE('',#1833,#1834,#1196,.T.);
#2235=EDGE_CURVE('',#1834,#1832,#1197,.T.);
#2236=EDGE_CURVE('',#1835,#1833,#1198,.T.);
#2237=EDGE_CURVE('',#1835,#1836,#1199,.T.);
#2238=EDGE_CURVE('',#1836,#1834,#1200,.T.);
#2239=EDGE_CURVE('',#1837,#1835,#1201,.T.);
#2240=EDGE_CURVE('',#1837,#1838,#1202,.T.);
#2241=EDGE_CURVE('',#1838,#1836,#1203,.T.);
#2242=EDGE_CURVE('',#1828,#1837,#1204,.T.);
#2243=EDGE_CURVE('',#1830,#1838,#1205,.T.);
#2244=EDGE_CURVE('',#1839,#1839,#1565,.T.);
#2245=EDGE_CURVE('',#1840,#1840,#1566,.T.);
#2246=EDGE_CURVE('',#1840,#1839,#1206,.T.);
#2247=EDGE_CURVE('',#1841,#1841,#1567,.F.);
#2248=EDGE_CURVE('',#1841,#1840,#1207,.T.);
#2249=EDGE_CURVE('',#1842,#1842,#1568,.T.);
#2250=EDGE_CURVE('',#1842,#1841,#1208,.T.);
#3017=ORIENTED_EDGE('',*,*,#2226,.F.);
#3018=ORIENTED_EDGE('',*,*,#2227,.T.);
#3019=ORIENTED_EDGE('',*,*,#2228,.T.);
#3020=ORIENTED_EDGE('',*,*,#2229,.F.);
#3021=ORIENTED_EDGE('',*,*,#2230,.F.);
#3022=ORIENTED_EDGE('',*,*,#2231,.T.);
#3023=ORIENTED_EDGE('',*,*,#2232,.T.);
#3024=ORIENTED_EDGE('',*,*,#2227,.F.);
#3025=ORIENTED_EDGE('',*,*,#2233,.F.);
#3026=ORIENTED_EDGE('',*,*,#2234,.T.);
#3027=ORIENTED_EDGE('',*,*,#2235,.T.);
#3028=ORIENTED_EDGE('',*,*,#2231,.F.);
#3029=ORIENTED_EDGE('',*,*,#2236,.F.);
#3030=ORIENTED_EDGE('',*,*,#2237,.T.);
#3031=ORIENTED_EDGE('',*,*,#2238,.T.);
#3032=ORIENTED_EDGE('',*,*,#2234,.F.);
#3033=ORIENTED_EDGE('',*,*,#2239,.F.);
#3034=ORIENTED_EDGE('',*,*,#2240,.T.);
#3035=ORIENTED_EDGE('',*,*,#2241,.T.);
#3036=ORIENTED_EDGE('',*,*,#2237,.F.);
#3037=ORIENTED_EDGE('',*,*,#2242,.F.);
#3038=ORIENTED_EDGE('',*,*,#2229,.T.);
#3039=ORIENTED_EDGE('',*,*,#2243,.T.);
#3040=ORIENTED_EDGE('',*,*,#2240,.F.);
#3041=ORIENTED_EDGE('',*,*,#2243,.F.);
#3042=ORIENTED_EDGE('',*,*,#2228,.F.);
#3043=ORIENTED_EDGE('',*,*,#2232,.F.);
#3044=ORIENTED_EDGE('',*,*,#2235,.F.);
#3045=ORIENTED_EDGE('',*,*,#2238,.F.);
#3046=ORIENTED_EDGE('',*,*,#2241,.F.);
#3047=ORIENTED_EDGE('',*,*,#2244,.F.);
#3048=ORIENTED_EDGE('',*,*,#2226,.T.);
#3049=ORIENTED_EDGE('',*,*,#2242,.T.);
#3050=ORIENTED_EDGE('',*,*,#2239,.T.);
#3051=ORIENTED_EDGE('',*,*,#2236,.T.);
#3052=ORIENTED_EDGE('',*,*,#2233,.T.);
#3053=ORIENTED_EDGE('',*,*,#2230,.T.);
#3054=ORIENTED_EDGE('',*,*,#2245,.F.);
#3055=ORIENTED_EDGE('',*,*,#2246,.T.);
#3056=ORIENTED_EDGE('',*,*,#2244,.T.);
#3057=ORIENTED_EDGE('',*,*,#2246,.F.);
#3058=ORIENTED_EDGE('',*,*,#2247,.F.);
#3059=ORIENTED_EDGE('',*,*,#2248,.T.);
#3060=ORIENTED_EDGE('',*,*,#2245,.T.);
#3061=ORIENTED_EDGE('',*,*,#2248,.F.);
#3062=ORIENTED_EDGE('',*,*,#2249,.F.);
#3063=ORIENTED_EDGE('',*,*,#2250,.T.);
#3064=ORIENTED_EDGE('',*,*,#2247,.T.);
#3065=ORIENTED_EDGE('',*,*,#2250,.F.);
#3066=ORIENTED_EDGE('',*,*,#2249,.T.);
#3131=CYLINDRICAL_SURFACE('',#3921,0.24505);
#3308=ADVANCED_FACE('',(#691),#506,.F.);
#3309=ADVANCED_FACE('',(#692),#507,.F.);
#3310=ADVANCED_FACE('',(#693),#508,.F.);
#3311=ADVANCED_FACE('',(#694),#509,.F.);
#3312=ADVANCED_FACE('',(#695),#510,.F.);
#3313=ADVANCED_FACE('',(#696),#511,.F.);
#3314=ADVANCED_FACE('',(#697),#512,.F.);
#3315=ADVANCED_FACE('',(#698,#409),#513,.T.);
#3316=ADVANCED_FACE('',(#699),#26,.T.);
#3317=ADVANCED_FACE('',(#700),#3131,.T.);
#3318=ADVANCED_FACE('',(#701),#27,.T.);
#3319=ADVANCED_FACE('',(#702),#514,.T.);
#3341=CLOSED_SHELL('',(#3308,#3309,#3310,#3311,#3312,#3313,#3314,#3315,
#3316,#3317,#3318,#3319));
#3909=AXIS2_PLACEMENT_3D('',#6692,#4857,#4858);
#3910=AXIS2_PLACEMENT_3D('',#6693,#4859,#4860);
#3911=AXIS2_PLACEMENT_3D('',#6702,#4865,#4866);
#3912=AXIS2_PLACEMENT_3D('',#6708,#4870,#4871);
#3913=AXIS2_PLACEMENT_3D('',#6714,#4875,#4876);
#3914=AXIS2_PLACEMENT_3D('',#6720,#4880,#4881);
#3915=AXIS2_PLACEMENT_3D('',#6726,#4885,#4886);
#3916=AXIS2_PLACEMENT_3D('',#6729,#4889,#4890);
#3917=AXIS2_PLACEMENT_3D('',#6730,#4891,#4892);
#3918=AXIS2_PLACEMENT_3D('',#6732,#4893,#4894);
#3919=AXIS2_PLACEMENT_3D('',#6733,#4895,#4896);
#3920=AXIS2_PLACEMENT_3D('',#6735,#4897,#4898);
#3921=AXIS2_PLACEMENT_3D('',#6737,#4900,#4901);
#3922=AXIS2_PLACEMENT_3D('',#6739,#4902,#4903);
#3923=AXIS2_PLACEMENT_3D('',#6741,#4905,#4906);
#3924=AXIS2_PLACEMENT_3D('',#6743,#4907,#4908);
#3925=AXIS2_PLACEMENT_3D('',#6745,#4910,#4911);
#4857=DIRECTION('axis',(0.,0.,1.));
#4858=DIRECTION('refdir',(1.,0.,0.));
#4859=DIRECTION('center_axis',(0.866025403784439,0.,-0.5));
#4860=DIRECTION('ref_axis',(0.5,0.,0.866025403784439));
#4861=DIRECTION('',(0.5,0.,0.866025403784439));
#4862=DIRECTION('',(0.,-1.,0.));
#4863=DIRECTION('',(0.5,0.,0.866025403784439));
#4864=DIRECTION('',(0.,-1.,0.));
#4865=DIRECTION('center_axis',(1.92296268638356E-16,0.,-1.));
#4866=DIRECTION('ref_axis',(1.,0.,1.92296268638356E-16));
#4867=DIRECTION('',(1.,0.,1.92296268638356E-16));
#4868=DIRECTION('',(0.,-1.,0.));
#4869=DIRECTION('',(1.,0.,1.92296268638356E-16));
#4870=DIRECTION('center_axis',(-0.866025403784439,0.,-0.5));
#4871=DIRECTION('ref_axis',(0.5,0.,-0.866025403784439));
#4872=DIRECTION('',(0.5,0.,-0.866025403784439));
#4873=DIRECTION('',(0.,-1.,0.));
#4874=DIRECTION('',(0.5,0.,-0.866025403784438));
#4875=DIRECTION('center_axis',(-0.866025403784439,0.,0.5));
#4876=DIRECTION('ref_axis',(-0.5,0.,-0.866025403784439));
#4877=DIRECTION('',(-0.5,0.,-0.866025403784439));
#4878=DIRECTION('',(0.,-1.,0.));
#4879=DIRECTION('',(-0.5,0.,-0.866025403784439));
#4880=DIRECTION('center_axis',(-1.92296268638356E-16,0.,1.));
#4881=DIRECTION('ref_axis',(-1.,0.,-1.92296268638356E-16));
#4882=DIRECTION('',(-1.,0.,-1.92296268638356E-16));
#4883=DIRECTION('',(0.,-1.,0.));
#4884=DIRECTION('',(-1.,0.,-1.92296268638356E-16));
#4885=DIRECTION('center_axis',(0.866025403784439,0.,0.5));
#4886=DIRECTION('ref_axis',(-0.5,0.,0.866025403784439));
#4887=DIRECTION('',(-0.5,0.,0.866025403784439));
#4888=DIRECTION('',(-0.5,0.,0.866025403784439));
#4889=DIRECTION('center_axis',(0.,-1.,0.));
#4890=DIRECTION('ref_axis',(0.,0.,-1.));
#4891=DIRECTION('center_axis',(0.,1.,0.));
#4892=DIRECTION('ref_axis',(0.,0.,1.));
#4893=DIRECTION('center_axis',(0.,-1.,0.));
#4894=DIRECTION('ref_axis',(1.,0.,0.));
#4895=DIRECTION('center_axis',(0.,-1.,0.));
#4896=DIRECTION('ref_axis',(1.,0.,0.));
#4897=DIRECTION('center_axis',(0.,-1.,0.));
#4898=DIRECTION('ref_axis',(1.,0.,0.));
#4899=DIRECTION('',(0.707106781186547,0.707106781186548,8.65956056235493E-17));
#4900=DIRECTION('center_axis',(0.,-1.,0.));
#4901=DIRECTION('ref_axis',(1.,0.,0.));
#4902=DIRECTION('center_axis',(0.,1.,0.));
#4903=DIRECTION('ref_axis',(1.,0.,0.));
#4904=DIRECTION('',(0.,1.,0.));
#4905=DIRECTION('center_axis',(0.,1.,0.));
#4906=DIRECTION('ref_axis',(1.,0.,0.));
#4907=DIRECTION('center_axis',(0.,-1.,0.));
#4908=DIRECTION('ref_axis',(1.,0.,0.));
#4909=DIRECTION('',(-0.707106781186547,0.707106781186548,-8.65956056235493E-17));
#4910=DIRECTION('center_axis',(0.,-1.,0.));
#4911=DIRECTION('ref_axis',(0.,0.,-1.));
#6692=CARTESIAN_POINT('',(0.,0.,0.));
#6693=CARTESIAN_POINT('Origin',(0.0721687836487032,0.,-0.125));
#6694=CARTESIAN_POINT('',(0.0721687836487032,0.,-0.125));
#6695=CARTESIAN_POINT('',(0.144337567297406,0.,0.));
#6696=CARTESIAN_POINT('',(0.117710979560879,0.,-0.0461186027918559));
#6697=CARTESIAN_POINT('',(0.0721687836487032,-0.25,-0.125));
#6698=CARTESIAN_POINT('',(0.0721687836487032,0.,-0.125));
#6699=CARTESIAN_POINT('',(0.144337567297406,-0.25,0.));
#6700=CARTESIAN_POINT('',(0.144337567297406,-0.25,0.));
#6701=CARTESIAN_POINT('',(0.144337567297406,0.,0.));
#6702=CARTESIAN_POINT('Origin',(-0.0721687836487032,0.,-0.125));
#6703=CARTESIAN_POINT('',(-0.0721687836487032,0.,-0.125));
#6704=CARTESIAN_POINT('',(0.0739156081756484,0.,-0.125));
#6705=CARTESIAN_POINT('',(-0.0721687836487032,-0.25,-0.125));
#6706=CARTESIAN_POINT('',(-0.0721687836487032,0.,-0.125));
#6707=CARTESIAN_POINT('',(0.0721687836487032,-0.25,-0.125));
#6708=CARTESIAN_POINT('Origin',(-0.144337567297406,0.,-4.16333634234434E-17));
#6709=CARTESIAN_POINT('',(-0.144337567297406,0.,-1.76762539787485E-17));
#6710=CARTESIAN_POINT('',(-0.0987953713852306,0.,-0.0788813972081442));
#6711=CARTESIAN_POINT('',(-0.144337567297406,-0.25,-2.77555756156289E-17));
#6712=CARTESIAN_POINT('',(-0.144337567297406,0.,-1.76762539787485E-17));
#6713=CARTESIAN_POINT('',(-0.0721687836487032,-0.25,-0.125));
#6714=CARTESIAN_POINT('Origin',(-0.0721687836487033,0.,0.125));
#6715=CARTESIAN_POINT('',(-0.0721687836487033,0.,0.125));
#6716=CARTESIAN_POINT('',(-0.0627109795608791,0.,0.141381397208144));
#6717=CARTESIAN_POINT('',(-0.0721687836487033,-0.25,0.125));
#6718=CARTESIAN_POINT('',(-0.0721687836487033,0.,0.125));
#6719=CARTESIAN_POINT('',(-0.144337567297406,-0.25,-1.76762539787485E-17));
#6720=CARTESIAN_POINT('Origin',(0.0721687836487032,0.,0.125));
#6721=CARTESIAN_POINT('',(0.0721687836487032,0.,0.125));
#6722=CARTESIAN_POINT('',(0.146084391824352,0.,0.125));
#6723=CARTESIAN_POINT('',(0.0721687836487032,-0.25,0.125));
#6724=CARTESIAN_POINT('',(0.0721687836487032,0.,0.125));
#6725=CARTESIAN_POINT('',(-0.0721687836487033,-0.25,0.125));
#6726=CARTESIAN_POINT('Origin',(0.144337567297406,0.,0.));
#6727=CARTESIAN_POINT('',(0.153795371385231,0.,-0.0163813972081441));
#6728=CARTESIAN_POINT('',(0.0721687836487032,-0.25,0.125));
#6729=CARTESIAN_POINT('Origin',(0.,-0.25,0.));
#6730=CARTESIAN_POINT('Origin',(0.22,0.,0.));
#6731=CARTESIAN_POINT('',(-0.22,-8.67361737988404E-18,-2.69422295812418E-17));
#6732=CARTESIAN_POINT('Origin',(0.,0.,0.));
#6733=CARTESIAN_POINT('Origin',(0.,-0.015,0.));
#6734=CARTESIAN_POINT('',(-0.24505,-0.02505,-3.00099698131059E-17));
#6735=CARTESIAN_POINT('Origin',(0.,-0.02505,0.));
#6736=CARTESIAN_POINT('',(-0.235,-0.015,-2.87791997799628E-17));
#6737=CARTESIAN_POINT('Origin',(0.,-0.3775,0.));
#6738=CARTESIAN_POINT('',(-0.24505,-0.72995,3.00099698131059E-17));
#6739=CARTESIAN_POINT('Origin',(0.,-0.72995,0.));
#6740=CARTESIAN_POINT('',(-0.24505,-0.3775,-3.00099698131059E-17));
#6741=CARTESIAN_POINT('Origin',(0.,-0.7625,0.));
#6742=CARTESIAN_POINT('',(-0.175,-0.8,-2.14313189850787E-17));
#6743=CARTESIAN_POINT('Origin',(0.,-0.8,0.));
#6744=CARTESIAN_POINT('',(-0.2125,-0.7625,-2.60237444818813E-17));
#6745=CARTESIAN_POINT('Origin',(0.,-0.8,0.));
#6779=UNCERTAINTY_MEASURE_WITH_UNIT(LENGTH_MEASURE(0.001),#6806,
'DISTANCE_ACCURACY_VALUE',
'Maximum model space distance between geometric entities at asserted c
onnectivities');
#6780=UNCERTAINTY_MEASURE_WITH_UNIT(LENGTH_MEASURE(0.001),#6806,
'DISTANCE_ACCURACY_VALUE',
'Maximum model space distance between geometric entities at asserted c
onnectivities');
#6804=(
GEOMETRIC_REPRESENTATION_CONTEXT(3)
GLOBAL_UNCERTAINTY_ASSIGNED_CONTEXT((#6779))
GLOBAL_UNIT_ASSIGNED_CONTEXT((#6806,#6808,#6809))
REPRESENTATION_CONTEXT('','3D')
);
#6805=(
GEOMETRIC_REPRESENTATION_CONTEXT(3)
GLOBAL_UNCERTAINTY_ASSIGNED_CONTEXT((#6780))
GLOBAL_UNIT_ASSIGNED_CONTEXT((#6806,#6808,#6809))
REPRESENTATION_CONTEXT('','3D')
);
#6806=(
LENGTH_UNIT()
NAMED_UNIT(*)
SI_UNIT(.CENTI.,.METRE.)
);
#6808=(
NAMED_UNIT(*)
PLANE_ANGLE_UNIT()
SI_UNIT($,.RADIAN.)
);
#6809=(
NAMED_UNIT(*)
SI_UNIT($,.STERADIAN.)
SOLID_ANGLE_UNIT()
);
#6833=SHAPE_DEFINITION_REPRESENTATION(#6887,#6921);
#6887=PRODUCT_DEFINITION_SHAPE('',$,#6946);
#6921=SHAPE_REPRESENTATION('',(#3909),#6804);
#6922=PRODUCT_DEFINITION_CONTEXT('part definition',#6996,'design');
#6946=PRODUCT_DEFINITION('Socket Set Screw - M5x8',
'Socket Set Screw - M5x8',#6970,#6922);
#6970=PRODUCT_DEFINITION_FORMATION('',$,#7021);
#6996=APPLICATION_CONTEXT(
'Core Data for Automotive Mechanical Design Process');
#6997=PRODUCT_CONTEXT('part definition',#6996,'mechanical');
#7021=PRODUCT('Socket Set Screw - M5x8','Socket Set Screw - M5x8',
'Socket Set Screw - M5x8',(#6997));
#7092=COLOUR_RGB('Black',0.12,0.14,0.17);
#7093=FILL_AREA_STYLE_COLOUR('',#7092);
#7094=FILL_AREA_STYLE('',(#7093));
#7095=SURFACE_STYLE_FILL_AREA(#7094);
#7096=SURFACE_SIDE_STYLE('',(#7095));
#7097=SURFACE_STYLE_USAGE(.BOTH.,#7096);
#7098=PRESENTATION_STYLE_ASSIGNMENT((#7097));
ENDSEC;
END-ISO-10303-21;
